ISO-10303-21;
HEADER;
FILE_DESCRIPTION (('STEP AP214'),
    '1' );
FILE_NAME ('angular contact ball bearing_68_iso_ISO 15 ABB - 178 - 20,SI,NC,20_68.step',
    '2026-10-31T03:44:21',
    ( '' ),
    ( '' ),
    'SwSTEP 2.0',
    'SolidWorks 2026',
    '' );
FILE_SCHEMA (( 'AUTOMOTIVE_DESIGN' ));
ENDSEC;

DATA;
#17=AXIS2_PLACEMENT_3D ( 'NONE', #16816, #16917, #3571 ) ;
#30=CIRCLE ( 'NONE', #4409, 4.100000000000000533 ) ;
#33=CARTESIAN_POINT ( 'NONE',  ( 1.150000000000001688, 7.347880794884120722E-16, 6.000000000000000888 ) ) ;
#43=ORIENTED_EDGE ( 'NONE', *, *, #11589, .T. ) ;
#59=AXIS2_PLACEMENT_3D ( 'NONE', #5322, #457, #13965 ) ;
#154=ADVANCED_FACE ( 'NONE', ( #6013 ), #15557, .T. ) ;
#188=CARTESIAN_POINT ( 'NONE',  ( -20.63749999999999574, 0.000000000000000000, 0.000000000000000000 ) ) ;
#222=EDGE_CURVE ( 'NONE', #2993, #6110, #13306, .T. ) ;
#228=VERTEX_POINT ( 'NONE', #12449 ) ;
#242=FACE_OUTER_BOUND ( 'NONE', #17390, .T. ) ;
#316=AXIS2_PLACEMENT_3D ( 'NONE', #4750, #1802, #7770 ) ;
#326=DIRECTION ( 'NONE',  ( 1.000000000000000000, 0.000000000000000000, 0.000000000000000000 ) ) ;
#333=FACE_OUTER_BOUND ( 'NONE', #13418, .T. ) ;
#338=CARTESIAN_POINT ( 'NONE',  ( -1.150000000000001688, 0.000000000000000000, -6.000000000000001776 ) ) ;
#356=ORIENTED_EDGE ( 'NONE', *, *, #17810, .F. ) ;
#357=DIRECTION ( 'NONE',  ( 0.000000000000000000, 0.000000000000000000, -1.000000000000000000 ) ) ;
#361=EDGE_CURVE ( 'NONE', #6066, #19035, #785, .T. ) ;
#378=ORIENTED_EDGE ( 'NONE', *, *, #13840, .F. ) ;
#384=ORIENTED_EDGE ( 'NONE', *, *, #11180, .F. ) ;
#420=DIRECTION ( 'NONE',  ( 0.000000000000000000, 0.000000000000000000, -1.000000000000000000 ) ) ;
#430=CYLINDRICAL_SURFACE ( 'NONE', #1391, 4.599999999999999645 ) ;
#444=VERTEX_POINT ( 'NONE', #3022 ) ;
#457=DIRECTION ( 'NONE',  ( 1.000000000000000000, 0.000000000000000000, 0.000000000000000000 ) ) ;
#524=CLOSED_SHELL ( 'NONE', ( #18637, #2934, #16284, #12275, #14309, #14146, #154, #5266, #18554, #3627, #6437, #13698, #10989, #17442, #12734, #18525, #12549, #4182, #11198, #4505, #11360, #6999, #9794, #15649, #16358, #2837, #940, #9380 ) ) ;
#529=AXIS2_PLACEMENT_3D ( 'NONE', #13472, #9051, #19389 ) ;
#582=DIRECTION ( 'NONE',  ( 1.000000000000000000, 0.000000000000000000, 0.000000000000000000 ) ) ;
#639=EDGE_LOOP ( 'NONE', ( #2645, #1504, #14829, #11525 ) ) ;
#665=CIRCLE ( 'NONE', #9128, 0.1000000000000011297 ) ;
#692=CARTESIAN_POINT ( 'NONE',  ( 0.000000000000000000, 6.123233995736766282E-16, -5.000000000000000000 ) ) ;
#697=CARTESIAN_POINT ( 'NONE',  ( -1.249999999999997558, 0.000000000000000000, 0.000000000000000000 ) ) ;
#705=DIRECTION ( 'NONE',  ( 0.000000000000000000, 0.000000000000000000, -1.000000000000000000 ) ) ;
#785=CIRCLE ( 'NONE', #2368, 4.599999999999999645 ) ;
#818=CIRCLE ( 'NONE', #16168, 5.400000000000000355 ) ;
#828=VERTEX_POINT ( 'NONE', #19294 ) ;
#831=CARTESIAN_POINT ( 'NONE',  ( -1.250000000000001110, 0.000000000000000000, 0.000000000000000000 ) ) ;
#901=CARTESIAN_POINT ( 'NONE',  ( -1.150000000000000577, 0.000000000000000000, 0.000000000000000000 ) ) ;
#940=ADVANCED_FACE ( 'NONE', ( #4362, #16332 ), #1714, .T. ) ;
#947=CARTESIAN_POINT ( 'NONE',  ( 1.250000000000001110, 0.000000000000000000, -5.400000000000000355 ) ) ;
#951=LINE ( 'NONE', #6923, #5911 ) ;
#963=CARTESIAN_POINT ( 'NONE',  ( -1.149999999999998135, 0.000000000000000000, 0.000000000000000000 ) ) ;
#989=CIRCLE ( 'NONE', #8166, 5.575000000000000178 ) ;
#1059=LINE ( 'NONE', #4191, #14747 ) ;
#1079=ORIENTED_EDGE ( 'NONE', *, *, #7115, .T. ) ;
#1099=DIRECTION ( 'NONE',  ( 0.000000000000000000, 0.000000000000000000, -1.000000000000000000 ) ) ;
#1158=LINE ( 'NONE', #1450, #1173 ) ;
#1173=VECTOR ( 'NONE', #10358, 1000.000000000000000 ) ;
#1199=DIRECTION ( 'NONE',  ( 0.000000000000000000, -1.000000000000000000, 0.000000000000000000 ) ) ;
#1211=CARTESIAN_POINT ( 'NONE',  ( -1.249999999999997558, 0.000000000000000000, -4.599999999999999645 ) ) ;
#1212=ORIENTED_EDGE ( 'NONE', *, *, #16769, .F. ) ;
#1231=COLOUR_RGB ( '',1.000000000000000000, 0.9490196078431372140, 0.9098039215686274384 ) ;
#1235=FACE_BOUND ( 'NONE', #16760, .T. ) ;
#1252=DIRECTION ( 'NONE',  ( 1.000000000000000000, 0.000000000000000000, 0.000000000000000000 ) ) ;
#1264=DIRECTION ( 'NONE',  ( 1.000000000000000000, 0.000000000000000000, 0.000000000000000000 ) ) ;
#1293=CARTESIAN_POINT ( 'NONE',  ( 1.249999999999997780, 0.000000000000000000, -4.100000000000000533 ) ) ;
#1310=CARTESIAN_POINT ( 'NONE',  ( -20.63749999999999929, 0.000000000000000000, 0.000000000000000000 ) ) ;
#1322=DIRECTION ( 'NONE',  ( 1.000000000000000000, 0.000000000000000000, 0.000000000000000000 ) ) ;
#1335=LINE ( 'NONE', #9059, #7854 ) ;
#1336=DIRECTION ( 'NONE',  ( 1.000000000000000000, 0.000000000000000000, 0.000000000000000000 ) ) ;
#1367=DIRECTION ( 'NONE',  ( 0.000000000000000000, 0.000000000000000000, -1.000000000000000000 ) ) ;
#1391=AXIS2_PLACEMENT_3D ( 'NONE', #3560, #9620, #15615 ) ;
#1444=DIRECTION ( 'NONE',  ( 1.000000000000000000, 0.000000000000000000, 0.000000000000000000 ) ) ;
#1450=CARTESIAN_POINT ( 'NONE',  ( -20.63749999999999574, 0.000000000000000000, -5.400000000000000355 ) ) ;
#1453=CYLINDRICAL_SURFACE ( 'NONE', #5994, 4.424999999999999822 ) ;
#1455=ORIENTED_EDGE ( 'NONE', *, *, #10708, .T. ) ;
#1459=( NAMED_UNIT ( * ) PLANE_ANGLE_UNIT ( ) SI_UNIT ( $, .RADIAN. ) );
#1471=PRODUCT_DEFINITION_SHAPE ( 'NONE', 'NONE',  #12013 ) ;
#1489=AXIS2_PLACEMENT_3D ( 'NONE', #2753, #10173, #11646 ) ;
#1504=ORIENTED_EDGE ( 'NONE', *, *, #16769, .T. ) ;
#1545=FACE_OUTER_BOUND ( 'NONE', #5227, .T. ) ;
#1554=CARTESIAN_POINT ( 'NONE',  ( -20.63749999999999929, 0.000000000000000000, 0.000000000000000000 ) ) ;
#1557=( GEOMETRIC_REPRESENTATION_CONTEXT ( 3 ) GLOBAL_UNCERTAINTY_ASSIGNED_CONTEXT ( ( #18148 ) ) GLOBAL_UNIT_ASSIGNED_CONTEXT ( ( #18375, #4921, #15504 ) ) REPRESENTATION_CONTEXT ( 'NONE', 'WORKASPACE' ) );
#1661=ORIENTED_EDGE ( 'NONE', *, *, #11349, .F. ) ;
#1676=DIRECTION ( 'NONE',  ( 0.000000000000000000, 0.000000000000000000, -1.000000000000000000 ) ) ;
#1701=PRESENTATION_STYLE_ASSIGNMENT (( #4745 ) ) ;
#1714=PLANE ( 'NONE',  #11650 ) ;
#1769=CARTESIAN_POINT ( 'NONE',  ( -1.249999999999997780, 5.021051876504148371E-16, 4.100000000000000533 ) ) ;
#1779=DIRECTION ( 'NONE',  ( 0.000000000000000000, 0.000000000000000000, -1.000000000000000000 ) ) ;
#1795=DIRECTION ( 'NONE',  ( 1.000000000000000000, 0.000000000000000000, 0.000000000000000000 ) ) ;
#1802=DIRECTION ( 'NONE',  ( 1.000000000000000000, 0.000000000000000000, 0.000000000000000000 ) ) ;
#1820=DIRECTION ( 'NONE',  ( 1.000000000000000000, 0.000000000000000000, 0.000000000000000000 ) ) ;
#1845=CARTESIAN_POINT ( 'NONE',  ( 0.000000000000000000, 6.123233995736766282E-16, -5.000000000000000000 ) ) ;
#1865=FACE_BOUND ( 'NONE', #3419, .T. ) ;
#1872=ORIENTED_EDGE ( 'NONE', *, *, #3635, .F. ) ;
#1876=AXIS2_PLACEMENT_3D ( 'NONE', #10314, #5518, #10685 ) ;
#1883=DIRECTION ( 'NONE',  ( -1.000000000000000000, -0.000000000000000000, -0.000000000000000000 ) ) ;
#1924=ORIENTED_EDGE ( 'NONE', *, *, #13332, .T. ) ;
#1927=ORIENTED_EDGE ( 'NONE', *, *, #10034, .T. ) ;
#1947=CARTESIAN_POINT ( 'NONE',  ( 0.000000000000000000, 0.000000000000000000, 0.000000000000000000 ) ) ;
#1949=AXIS2_PLACEMENT_3D ( 'NONE', #3122, #18123, #7519 ) ;
#1961=CARTESIAN_POINT ( 'NONE',  ( -1.249999999999998002, 4.599999999999999645, 0.000000000000000000 ) ) ;
#1963=CARTESIAN_POINT ( 'NONE',  ( -1.249999999999997558, 5.633375276077824112E-16, 4.599999999999999645 ) ) ;
#2012=EDGE_LOOP ( 'NONE', ( #9876, #7914, #1924, #13543 ) ) ;
#2085=DIRECTION ( 'NONE',  ( 0.000000000000000000, 0.000000000000000000, -1.000000000000000000 ) ) ;
#2086=CARTESIAN_POINT ( 'NONE',  ( 0.000000000000000000, 0.000000000000000000, 0.000000000000000000 ) ) ;
#2089=DIRECTION ( 'NONE',  ( 1.000000000000000000, 0.000000000000000000, 0.000000000000000000 ) ) ;
#2190=LINE ( 'NONE', #5406, #18794 ) ;
#2204=DIRECTION ( 'NONE',  ( 0.000000000000000000, -1.000000000000000000, 0.000000000000000000 ) ) ;
#2225=AXIS2_PLACEMENT_3D ( 'NONE', #14400, #14694, #5880 ) ;
#2236=AXIS2_PLACEMENT_3D ( 'NONE', #16897, #15123, #420 ) ;
#2252=ORIENTED_EDGE ( 'NONE', *, *, #11901, .T. ) ;
#2286=CARTESIAN_POINT ( 'NONE',  ( 0.1713913650100259145, 0.000000000000000000, 0.000000000000000000 ) ) ;
#2296=VERTEX_POINT ( 'NONE', #17836 ) ;
#2368=AXIS2_PLACEMENT_3D ( 'NONE', #697, #6958, #17567 ) ;
#2369=VERTEX_POINT ( 'NONE', #18419 ) ;
#2387=AXIS2_PLACEMENT_3D ( 'NONE', #17950, #10465, #3037 ) ;
#2477=EDGE_CURVE ( 'NONE', #12254, #7385, #7260, .T. ) ;
#2506=MECHANICAL_DESIGN_GEOMETRIC_PRESENTATION_REPRESENTATION('',(#15318),#3133);
#2644=DIRECTION ( 'NONE',  ( 0.000000000000000000, -1.224646799147353207E-16, 1.000000000000000000 ) ) ;
#2645=ORIENTED_EDGE ( 'NONE', *, *, #17075, .T. ) ;
#2647=VERTEX_POINT ( 'NONE', #33 ) ;
#2667=DIRECTION ( 'NONE',  ( 1.000000000000000000, 0.000000000000000000, 0.000000000000000000 ) ) ;
#2733=ORIENTED_EDGE ( 'NONE', *, *, #13332, .F. ) ;
#2753=CARTESIAN_POINT ( 'NONE',  ( 1.149999999999998135, 0.000000000000000000, 0.000000000000000000 ) ) ;
#2837=ADVANCED_FACE ( 'NONE', ( #13207 ), #6022, .T. ) ;
#2843=VERTEX_POINT ( 'NONE', #18653 ) ;
#2852=CIRCLE ( 'NONE', #2236, 5.899999999999999467 ) ;
#2871=CARTESIAN_POINT ( 'NONE',  ( 0.000000000000000000, 0.000000000000000000, 0.000000000000000000 ) ) ;
#2879=CIRCLE ( 'NONE', #12555, 4.424999999999999822 ) ;
#2907=DIRECTION ( 'NONE',  ( 1.000000000000000000, 0.000000000000000000, 0.000000000000000000 ) ) ;
#2915=CARTESIAN_POINT ( 'NONE',  ( 0.000000000000000000, 0.000000000000000000, 0.000000000000000000 ) ) ;
#2934=ADVANCED_FACE ( 'NONE', ( #1545 ), #3305, .T. ) ;
#2966=FACE_OUTER_BOUND ( 'NONE', #12713, .T. ) ;
#2993=VERTEX_POINT ( 'NONE', #6143 ) ;
#3005=CARTESIAN_POINT ( 'NONE',  ( 1.249999999999998002, 4.100000000000000533, 0.000000000000000000 ) ) ;
#3022=CARTESIAN_POINT ( 'NONE',  ( -1.249999999999997780, 0.000000000000000000, -4.100000000000000533 ) ) ;
#3035=( LENGTH_UNIT ( ) NAMED_UNIT ( * ) SI_UNIT ( .MILLI., .METRE. ) );
#3037=DIRECTION ( 'NONE',  ( 0.000000000000000000, 1.224646799147353207E-16, 1.000000000000000000 ) ) ;
#3122=CARTESIAN_POINT ( 'NONE',  ( -20.63749999999999574, 0.000000000000000000, 0.000000000000000000 ) ) ;
#3133=( GEOMETRIC_REPRESENTATION_CONTEXT ( 3 ) GLOBAL_UNCERTAINTY_ASSIGNED_CONTEXT ( ( #15183 ) ) GLOBAL_UNIT_ASSIGNED_CONTEXT ( ( #17088, #6579, #13650 ) ) REPRESENTATION_CONTEXT ( 'NONE', 'WORKASPACE' ) );
#3175=CARTESIAN_POINT ( 'NONE',  ( 1.249999999999997558, 5.419062086227038392E-16, 4.424999999999999822 ) ) ;
#3191=ORIENTED_EDGE ( 'NONE', *, *, #7720, .F. ) ;
#3201=DIRECTION ( 'NONE',  ( 1.000000000000000000, 0.000000000000000000, 0.000000000000000000 ) ) ;
#3210=CARTESIAN_POINT ( 'NONE',  ( -1.150000000000000577, 0.000000000000000000, 0.000000000000000000 ) ) ;
#3228=VERTEX_POINT ( 'NONE', #7099 ) ;
#3305=CYLINDRICAL_SURFACE ( 'NONE', #1949, 6.000000000000001776 ) ;
#3354=CIRCLE ( 'NONE', #529, 4.424999999999999822 ) ;
#3379=CARTESIAN_POINT ( 'NONE',  ( -20.63749999999999574, 0.000000000000000000, 0.000000000000000000 ) ) ;
#3419=EDGE_LOOP ( 'NONE', ( #18617, #9090 ) ) ;
#3445=CARTESIAN_POINT ( 'NONE',  ( 1.250000000000001110, 0.000000000000000000, 0.000000000000000000 ) ) ;
#3458=CIRCLE ( 'NONE', #17, 6.000000000000000888 ) ;
#3484=ORIENTED_EDGE ( 'NONE', *, *, #7051, .F. ) ;
#3560=CARTESIAN_POINT ( 'NONE',  ( -20.63749999999999929, 0.000000000000000000, 0.000000000000000000 ) ) ;
#3571=DIRECTION ( 'NONE',  ( 0.000000000000000000, 0.000000000000000000, -1.000000000000000000 ) ) ;
#3572=AXIS2_PLACEMENT_3D ( 'NONE', #19071, #15818, #5613 ) ;
#3603=ORIENTED_EDGE ( 'NONE', *, *, #15982, .T. ) ;
#3627=ADVANCED_FACE ( 'NONE', ( #9527 ), #430, .T. ) ;
#3635=EDGE_CURVE ( 'NONE', #6110, #444, #10769, .T. ) ;
#3642=EDGE_CURVE ( 'NONE', #16030, #3706, #13935, .T. ) ;
#3677=ORIENTED_EDGE ( 'NONE', *, *, #11589, .F. ) ;
#3706=VERTEX_POINT ( 'NONE', #8252 ) ;
#3722=EDGE_LOOP ( 'NONE', ( #19194, #9901 ) ) ;
#3848=FACE_OUTER_BOUND ( 'NONE', #3950, .T. ) ;
#3858=CYLINDRICAL_SURFACE ( 'NONE', #10140, 4.000000000000000000 ) ;
#3877=ORIENTED_EDGE ( 'NONE', *, *, #3642, .T. ) ;
#3886=EDGE_CURVE ( 'NONE', #12017, #2369, #13345, .T. ) ;
#3899=ORIENTED_EDGE ( 'NONE', *, *, #11297, .T. ) ;
#3906=DIRECTION ( 'NONE',  ( 1.000000000000000000, 0.000000000000000000, 0.000000000000000000 ) ) ;
#3932=CARTESIAN_POINT ( 'NONE',  ( -20.63749999999999929, 0.000000000000000000, 0.000000000000000000 ) ) ;
#3940=DIRECTION ( 'NONE',  ( -1.000000000000000000, -0.000000000000000000, -0.000000000000000000 ) ) ;
#3950=EDGE_LOOP ( 'NONE', ( #1455, #16464, #13611, #3677 ) ) ;
#3978=CARTESIAN_POINT ( 'NONE',  ( 1.249999999999997558, 0.000000000000000000, 0.000000000000000000 ) ) ;
#4035=DIRECTION ( 'NONE',  ( 1.000000000000000000, 0.000000000000000000, 0.000000000000000000 ) ) ;
#4061=ORIENTED_EDGE ( 'NONE', *, *, #11180, .T. ) ;
#4064=AXIS2_PLACEMENT_3D ( 'NONE', #8932, #1199, #1099 ) ;
#4067=EDGE_LOOP ( 'NONE', ( #1661, #8705, #14473, #11743 ) ) ;
#4079=CARTESIAN_POINT ( 'NONE',  ( 0.000000000000000000, 0.000000000000000000, 5.000000000000000000 ) ) ;
#4095=ORIENTED_EDGE ( 'NONE', *, *, #16710, .F. ) ;
#4117=ORIENTED_EDGE ( 'NONE', *, *, #17810, .T. ) ;
#4138=SHAPE_DEFINITION_REPRESENTATION ( #1471, #18081 ) ;
#4145=CARTESIAN_POINT ( 'NONE',  ( 0.4472135954999577612, 6.613092715395707467E-16, -5.400000000000000355 ) ) ;
#4182=ADVANCED_FACE ( 'NONE', ( #15987 ), #13137, .F. ) ;
#4191=CARTESIAN_POINT ( 'NONE',  ( -20.63749999999999929, 5.419062086227038392E-16, 4.424999999999999822 ) ) ;
#4241=DIRECTION ( 'NONE',  ( 1.000000000000000000, 0.000000000000000000, 0.000000000000000000 ) ) ;
#4253=CARTESIAN_POINT ( 'NONE',  ( 1.150000000000001688, 0.000000000000000000, 0.000000000000000000 ) ) ;
#4348=ORIENTED_EDGE ( 'NONE', *, *, #3642, .F. ) ;
#4362=FACE_OUTER_BOUND ( 'NONE', #3722, .T. ) ;
#4403=AXIS2_PLACEMENT_3D ( 'NONE', #16645, #11917, #12014 ) ;
#4409=AXIS2_PLACEMENT_3D ( 'NONE', #5912, #10413, #17692 ) ;
#4420=EDGE_CURVE ( 'NONE', #12017, #2993, #14861, .T. ) ;
#4423=LINE ( 'NONE', #18155, #6931 ) ;
#4435=FACE_BOUND ( 'NONE', #6746, .T. ) ;
#4453=PRODUCT ( 'angular contact ball bearing_68_iso_ISO 15 ABB - 178 - 20,SI,NC,20_68', 'angular contact ball bearing_68_iso_ISO 15 ABB - 178 - 20,SI,NC,20_68', '', ( #5794 ) ) ;
#4505=ADVANCED_FACE ( 'NONE', ( #1865, #10859 ), #13894, .T. ) ;
#4533=CARTESIAN_POINT ( 'NONE',  ( -20.63749999999999929, 5.633375276077824112E-16, 4.599999999999999645 ) ) ;
#4578=AXIS2_PLACEMENT_3D ( 'NONE', #188, #12135, #1367 ) ;
#4707=CARTESIAN_POINT ( 'NONE',  ( 1.250000000000001110, 0.000000000000000000, -5.899999999999999467 ) ) ;
#4719=CARTESIAN_POINT ( 'NONE',  ( -0.4472135954999577612, 0.000000000000000000, 0.000000000000000000 ) ) ;
#4730=DIRECTION ( 'NONE',  ( 0.000000000000000000, 1.000000000000000000, -1.224646799147353207E-16 ) ) ;
#4745=SURFACE_STYLE_USAGE ( .BOTH. , #16998 ) ;
#4750=CARTESIAN_POINT ( 'NONE',  ( -1.250000000000001110, 0.000000000000000000, 0.000000000000000000 ) ) ;
#4791=FACE_OUTER_BOUND ( 'NONE', #639, .T. ) ;
#4831=VECTOR ( 'NONE', #14029, 1000.000000000000000 ) ;
#4847=AXIS2_PLACEMENT_3D ( 'NONE', #1961, #10674, #12430 ) ;
#4892=EDGE_CURVE ( 'NONE', #19035, #16243, #8891, .T. ) ;
#4902=DIRECTION ( 'NONE',  ( 0.000000000000000000, 0.000000000000000000, -1.000000000000000000 ) ) ;
#4909=CARTESIAN_POINT ( 'NONE',  ( 0.1713913650100259145, 0.000000000000000000, 0.000000000000000000 ) ) ;
#4921=( NAMED_UNIT ( * ) PLANE_ANGLE_UNIT ( ) SI_UNIT ( $, .RADIAN. ) );
#4967=EDGE_LOOP ( 'NONE', ( #8752, #4061, #10105, #4978 ) ) ;
#4970=CARTESIAN_POINT ( 'NONE',  ( 0.4472135954999577612, 0.000000000000000000, 5.400000000000000355 ) ) ;
#4978=ORIENTED_EDGE ( 'NONE', *, *, #7115, .F. ) ;
#5012=AXIS2_PLACEMENT_3D ( 'NONE', #9247, #2204, #13068 ) ;
#5139=DIRECTION ( 'NONE',  ( -1.000000000000000000, -0.000000000000000000, -0.000000000000000000 ) ) ;
#5175=AXIS2_PLACEMENT_3D ( 'NONE', #15201, #13544, #1779 ) ;
#5227=EDGE_LOOP ( 'NONE', ( #11023, #7444, #11115, #18862 ) ) ;
#5265=DIRECTION ( 'NONE',  ( 1.000000000000000000, 0.000000000000000000, 0.000000000000000000 ) ) ;
#5266=ADVANCED_FACE ( 'NONE', ( #7181 ), #3858, .F. ) ;
#5291=DIRECTION ( 'NONE',  ( 1.000000000000000000, 0.000000000000000000, 0.000000000000000000 ) ) ;
#5311=EDGE_CURVE ( 'NONE', #8220, #15181, #9503, .T. ) ;
#5322=CARTESIAN_POINT ( 'NONE',  ( -1.150000000000001688, 0.000000000000000000, 0.000000000000000000 ) ) ;
#5369=DIRECTION ( 'NONE',  ( 1.000000000000000000, 0.000000000000000000, 0.000000000000000000 ) ) ;
#5406=CARTESIAN_POINT ( 'NONE',  ( -20.63749999999999574, 0.000000000000000000, -5.575000000000000178 ) ) ;
#5480=VERTEX_POINT ( 'NONE', #3175 ) ;
#5518=DIRECTION ( 'NONE',  ( -1.000000000000000000, -0.000000000000000000, -0.000000000000000000 ) ) ;
#5522=ORIENTED_EDGE ( 'NONE', *, *, #5927, .T. ) ;
#5558=CARTESIAN_POINT ( 'NONE',  ( 1.150000000000000577, 0.000000000000000000, 0.000000000000000000 ) ) ;
#5613=DIRECTION ( 'NONE',  ( 0.000000000000000000, 0.000000000000000000, -1.000000000000000000 ) ) ;
#5705=ORIENTED_EDGE ( 'NONE', *, *, #8789, .F. ) ;
#5740=DIRECTION ( 'NONE',  ( 0.000000000000000000, -1.000000000000000000, 0.000000000000000000 ) ) ;
#5747=DIRECTION ( 'NONE',  ( 0.000000000000000000, 0.000000000000000000, 1.000000000000000000 ) ) ;
#5758=ORIENTED_EDGE ( 'NONE', *, *, #11309, .F. ) ;
#5781=CARTESIAN_POINT ( 'NONE',  ( -1.150000000000001688, 0.000000000000000000, 0.000000000000000000 ) ) ;
#5794=PRODUCT_CONTEXT ( 'NONE', #8877, 'mechanical' ) ;
#5880=DIRECTION ( 'NONE',  ( 0.000000000000000000, 0.000000000000000000, -1.000000000000000000 ) ) ;
#5888=AXIS2_PLACEMENT_3D ( 'NONE', #3978, #2907, #11612 ) ;
#5911=VECTOR ( 'NONE', #17338, 1000.000000000000000 ) ;
#5912=CARTESIAN_POINT ( 'NONE',  ( -1.249999999999997558, 0.000000000000000000, 0.000000000000000000 ) ) ;
#5927=EDGE_CURVE ( 'NONE', #7385, #8711, #4423, .T. ) ;
#5994=AXIS2_PLACEMENT_3D ( 'NONE', #1554, #1264, #7431 ) ;
#6013=FACE_OUTER_BOUND ( 'NONE', #15349, .T. ) ;
#6014=CARTESIAN_POINT ( 'NONE',  ( -20.63749999999999929, 0.000000000000000000, -4.000000000000000000 ) ) ;
#6022=TOROIDAL_SURFACE ( 'NONE', #6945, 5.899999999999999467, 0.1000000000000010186 ) ;
#6025=ORIENTED_EDGE ( 'NONE', *, *, #18647, .F. ) ;
#6039=DIRECTION ( 'NONE',  ( 1.000000000000000000, 0.000000000000000000, 0.000000000000000000 ) ) ;
#6053=FACE_OUTER_BOUND ( 'NONE', #10844, .T. ) ;
#6066=VERTEX_POINT ( 'NONE', #1963 ) ;
#6078=ORIENTED_EDGE ( 'NONE', *, *, #18085, .F. ) ;
#6098=VECTOR ( 'NONE', #7276, 1000.000000000000000 ) ;
#6110=VERTEX_POINT ( 'NONE', #1769 ) ;
#6134=CARTESIAN_POINT ( 'NONE',  ( -0.1713913650100259145, 0.000000000000000000, 5.575000000000000178 ) ) ;
#6140=DIRECTION ( 'NONE',  ( -1.000000000000000000, -0.000000000000000000, -0.000000000000000000 ) ) ;
#6143=CARTESIAN_POINT ( 'NONE',  ( -1.149999999999998135, 4.898587196589412829E-16, 4.000000000000000000 ) ) ;
#6191=VECTOR ( 'NONE', #326, 1000.000000000000000 ) ;
#6211=ORIENTED_EDGE ( 'NONE', *, *, #19024, .F. ) ;
#6219=CARTESIAN_POINT ( 'NONE',  ( -0.4472135954999577612, 0.000000000000000000, 0.000000000000000000 ) ) ;
#6223=DIRECTION ( 'NONE',  ( 1.000000000000000000, 0.000000000000000000, 0.000000000000000000 ) ) ;
#6353=VERTEX_POINT ( 'NONE', #9968 ) ;
#6370=LINE ( 'NONE', #4533, #14080 ) ;
#6437=ADVANCED_FACE ( 'NONE', ( #8894 ), #1453, .T. ) ;
#6467=DIRECTION ( 'NONE',  ( 0.000000000000000000, 1.224646799147353207E-16, 1.000000000000000000 ) ) ;
#6528=AXIS2_PLACEMENT_3D ( 'NONE', #15950, #8289, #6823 ) ;
#6530=DIRECTION ( 'NONE',  ( -1.000000000000000000, -0.000000000000000000, -0.000000000000000000 ) ) ;
#6579=( NAMED_UNIT ( * ) PLANE_ANGLE_UNIT ( ) SI_UNIT ( $, .RADIAN. ) );
#6588=CIRCLE ( 'NONE', #17581, 4.424999999999999822 ) ;
#6601=CIRCLE ( 'NONE', #9425, 4.000000000000000000 ) ;
#6655=ORIENTED_EDGE ( 'NONE', *, *, #6993, .T. ) ;
#6667=DIRECTION ( 'NONE',  ( 1.000000000000000000, 0.000000000000000000, 0.000000000000000000 ) ) ;
#6680=VERTEX_POINT ( 'NONE', #11328 ) ;
#6722=ORIENTED_EDGE ( 'NONE', *, *, #13988, .F. ) ;
#6743=AXIS2_PLACEMENT_3D ( 'NONE', #14912, #12349, #14002 ) ;
#6746=EDGE_LOOP ( 'NONE', ( #17438, #14375 ) ) ;
#6822=ORIENTED_EDGE ( 'NONE', *, *, #19157, .T. ) ;
#6823=DIRECTION ( 'NONE',  ( 0.000000000000000000, 1.224646799147351975E-16, 1.000000000000000000 ) ) ;
#6842=EDGE_LOOP ( 'NONE', ( #14973, #7927 ) ) ;
#6869=EDGE_CURVE ( 'NONE', #9645, #15764, #1335, .T. ) ;
#6877=CARTESIAN_POINT ( 'NONE',  ( -1.149999999999998135, 0.000000000000000000, -4.100000000000000533 ) ) ;
#6892=CIRCLE ( 'NONE', #12213, 0.5999999999999998668 ) ;
#6914=AXIS2_PLACEMENT_3D ( 'NONE', #13666, #6223, #18206 ) ;
#6923=CARTESIAN_POINT ( 'NONE',  ( -20.63749999999999929, 4.898587196589412829E-16, 4.000000000000000000 ) ) ;
#6931=VECTOR ( 'NONE', #13623, 1000.000000000000000 ) ;
#6936=DIRECTION ( 'NONE',  ( 0.000000000000000000, 0.000000000000000000, -1.000000000000000000 ) ) ;
#6945=AXIS2_PLACEMENT_3D ( 'NONE', #5558, #6667, #17829 ) ;
#6958=DIRECTION ( 'NONE',  ( 1.000000000000000000, 0.000000000000000000, 0.000000000000000000 ) ) ;
#6973=CYLINDRICAL_SURFACE ( 'NONE', #9686, 6.000000000000001776 ) ;
#6993=EDGE_CURVE ( 'NONE', #3706, #5480, #2879, .T. ) ;
#6999=ADVANCED_FACE ( 'NONE', ( #242 ), #9342, .F. ) ;
#7051=EDGE_CURVE ( 'NONE', #17538, #2843, #16335, .T. ) ;
#7063=CARTESIAN_POINT ( 'NONE',  ( -20.63749999999999574, 6.613092715395707467E-16, 5.400000000000000355 ) ) ;
#7099=CARTESIAN_POINT ( 'NONE',  ( -1.250000000000001110, 0.000000000000000000, -5.575000000000000178 ) ) ;
#7115=EDGE_CURVE ( 'NONE', #828, #2369, #19168, .T. ) ;
#7181=FACE_OUTER_BOUND ( 'NONE', #17594, .T. ) ;
#7196=AXIS2_PLACEMENT_3D ( 'NONE', #3005, #13192, #10432 ) ;
#7255=DIRECTION ( 'NONE',  ( 0.000000000000000000, -1.000000000000000000, 0.000000000000000000 ) ) ;
#7260=CIRCLE ( 'NONE', #59, 6.000000000000001776 ) ;
#7276=DIRECTION ( 'NONE',  ( 1.000000000000000000, 0.000000000000000000, 0.000000000000000000 ) ) ;
#7296=CARTESIAN_POINT ( 'NONE',  ( -1.149999999999998135, 0.000000000000000000, -4.000000000000000000 ) ) ;
#7310=DIRECTION ( 'NONE',  ( 0.000000000000000000, 0.000000000000000000, -1.000000000000000000 ) ) ;
#7385=VERTEX_POINT ( 'NONE', #338 ) ;
#7431=DIRECTION ( 'NONE',  ( 0.000000000000000000, 0.000000000000000000, -1.000000000000000000 ) ) ;
#7444=ORIENTED_EDGE ( 'NONE', *, *, #12644, .T. ) ;
#7476=AXIS2_PLACEMENT_3D ( 'NONE', #14266, #9661, #17136 ) ;
#7506=FACE_OUTER_BOUND ( 'NONE', #2012, .T. ) ;
#7519=DIRECTION ( 'NONE',  ( 0.000000000000000000, 0.000000000000000000, -1.000000000000000000 ) ) ;
#7532=CIRCLE ( 'NONE', #17888, 6.000000000000001776 ) ;
#7565=CARTESIAN_POINT ( 'NONE',  ( -1.149999999999998135, 0.000000000000000000, 0.000000000000000000 ) ) ;
#7594=CARTESIAN_POINT ( 'NONE',  ( 1.249999999999997558, 0.000000000000000000, 0.000000000000000000 ) ) ;
#7601=ORIENTED_EDGE ( 'NONE', *, *, #13930, .F. ) ;
#7651=ORIENTED_EDGE ( 'NONE', *, *, #16710, .T. ) ;
#7720=EDGE_CURVE ( 'NONE', #12017, #444, #14605, .T. ) ;
#7770=DIRECTION ( 'NONE',  ( 0.000000000000000000, 0.000000000000000000, -1.000000000000000000 ) ) ;
#7819=CIRCLE ( 'NONE', #316, 5.575000000000000178 ) ;
#7850=DIRECTION ( 'NONE',  ( 0.000000000000000000, 0.000000000000000000, 1.000000000000000000 ) ) ;
#7853=AXIS2_PLACEMENT_3D ( 'NONE', #2086, #10894, #17002 ) ;
#7854=VECTOR ( 'NONE', #16145, 1000.000000000000000 ) ;
#7888=CYLINDRICAL_SURFACE ( 'NONE', #14047, 5.400000000000000355 ) ;
#7914=ORIENTED_EDGE ( 'NONE', *, *, #13840, .T. ) ;
#7927=ORIENTED_EDGE ( 'NONE', *, *, #11062, .F. ) ;
#8019=ORIENTED_EDGE ( 'NONE', *, *, #10638, .T. ) ;
#8054=CARTESIAN_POINT ( 'NONE',  ( -20.63749999999999929, 0.000000000000000000, -4.424999999999999822 ) ) ;
#8066=DIRECTION ( 'NONE',  ( 1.000000000000000000, 0.000000000000000000, 0.000000000000000000 ) ) ;
#8095=TOROIDAL_SURFACE ( 'NONE', #16277, 5.000000000000000000, 0.5999999999999999778 ) ;
#8149=CARTESIAN_POINT ( 'NONE',  ( -0.1713913650100259145, 6.827405905246493187E-16, -5.575000000000000178 ) ) ;
#8158=CARTESIAN_POINT ( 'NONE',  ( -1.249999999999997558, 0.000000000000000000, 0.000000000000000000 ) ) ;
#8166=AXIS2_PLACEMENT_3D ( 'NONE', #10252, #5369, #9865 ) ;
#8205=ORIENTED_EDGE ( 'NONE', *, *, #16944, .F. ) ;
#8206=ORIENTED_EDGE ( 'NONE', *, *, #10708, .F. ) ;
#8210=ORIENTED_EDGE ( 'NONE', *, *, #3886, .F. ) ;
#8212=ORIENTED_EDGE ( 'NONE', *, *, #222, .F. ) ;
#8220=VERTEX_POINT ( 'NONE', #8602 ) ;
#8234=ADVANCED_BREP_SHAPE_REPRESENTATION ( '', ( #14979, #10359 ), #1557 ) ;
#8239=DIRECTION ( 'NONE',  ( 0.000000000000000000, 0.000000000000000000, 1.000000000000000000 ) ) ;
#8244=EDGE_CURVE ( 'NONE', #18044, #18478, #1158, .T. ) ;
#8245=DIRECTION ( 'NONE',  ( 0.000000000000000000, 0.000000000000000000, -1.000000000000000000 ) ) ;
#8252=CARTESIAN_POINT ( 'NONE',  ( 1.249999999999997558, 0.000000000000000000, -4.424999999999999822 ) ) ;
#8289=DIRECTION ( 'NONE',  ( 0.000000000000000000, 1.000000000000000000, -1.224646799147353207E-16 ) ) ;
#8361=EDGE_LOOP ( 'NONE', ( #14388, #9636, #9561, #12686 ) ) ;
#8461=DIRECTION ( 'NONE',  ( 0.000000000000000000, 0.000000000000000000, -1.000000000000000000 ) ) ;
#8473=DIRECTION ( 'NONE',  ( 1.000000000000000000, 0.000000000000000000, 0.000000000000000000 ) ) ;
#8570=ORIENTED_EDGE ( 'NONE', *, *, #18647, .T. ) ;
#8602=CARTESIAN_POINT ( 'NONE',  ( 0.1713913650100259145, 0.000000000000000000, 4.424999999999999822 ) ) ;
#8620=DIRECTION ( 'NONE',  ( 0.000000000000000000, 0.000000000000000000, -1.000000000000000000 ) ) ;
#8657=DIRECTION ( 'NONE',  ( 0.000000000000000000, 0.000000000000000000, -1.000000000000000000 ) ) ;
#8659=AXIS2_PLACEMENT_3D ( 'NONE', #6877, #7255, #13229 ) ;
#8662=ORIENTED_EDGE ( 'NONE', *, *, #8673, .T. ) ;
#8673=EDGE_CURVE ( 'NONE', #15764, #6353, #17775, .T. ) ;
#8705=ORIENTED_EDGE ( 'NONE', *, *, #18085, .T. ) ;
#8711=VERTEX_POINT ( 'NONE', #17419 ) ;
#8713=EDGE_CURVE ( 'NONE', #18086, #2296, #10869, .T. ) ;
#8718=CYLINDRICAL_SURFACE ( 'NONE', #2225, 4.424999999999999822 ) ;
#8733=AXIS2_PLACEMENT_3D ( 'NONE', #1845, #16752, #13792 ) ;
#8752=ORIENTED_EDGE ( 'NONE', *, *, #9762, .F. ) ;
#8771=CIRCLE ( 'NONE', #10008, 4.424999999999999822 ) ;
#8789=EDGE_CURVE ( 'NONE', #6353, #16243, #15273, .T. ) ;
#8834=DIRECTION ( 'NONE',  ( 0.000000000000000000, 0.000000000000000000, 1.000000000000000000 ) ) ;
#8859=EDGE_LOOP ( 'NONE', ( #18492, #16534, #11305, #356 ) ) ;
#8877=APPLICATION_CONTEXT ( 'automotive_design' ) ;
#8891=LINE ( 'NONE', #14674, #14877 ) ;
#8894=FACE_OUTER_BOUND ( 'NONE', #17719, .T. ) ;
#8930=PLANE ( 'NONE',  #6743 ) ;
#8932=CARTESIAN_POINT ( 'NONE',  ( 1.149999999999998135, 0.000000000000000000, -4.100000000000000533 ) ) ;
#9037=CIRCLE ( 'NONE', #6528, 0.1000000000000011297 ) ;
#9046=ORIENTED_EDGE ( 'NONE', *, *, #5311, .T. ) ;
#9051=DIRECTION ( 'NONE',  ( 1.000000000000000000, 0.000000000000000000, 0.000000000000000000 ) ) ;
#9059=CARTESIAN_POINT ( 'NONE',  ( -20.63749999999999574, 6.827405905246494173E-16, 5.575000000000000178 ) ) ;
#9075=CARTESIAN_POINT ( 'NONE',  ( 0.000000000000000000, 0.000000000000000000, 0.000000000000000000 ) ) ;
#9090=ORIENTED_EDGE ( 'NONE', *, *, #3635, .T. ) ;
#9128=AXIS2_PLACEMENT_3D ( 'NONE', #15443, #16832, #15739 ) ;
#9168=EDGE_LOOP ( 'NONE', ( #6025, #18597 ) ) ;
#9210=ORIENTED_EDGE ( 'NONE', *, *, #11304, .F. ) ;
#9240=CARTESIAN_POINT ( 'NONE',  ( 1.250000000000000666, 5.899999999999999467, 0.000000000000000000 ) ) ;
#9247=CARTESIAN_POINT ( 'NONE',  ( 1.150000000000000577, 0.000000000000000000, -5.899999999999999467 ) ) ;
#9282=CYLINDRICAL_SURFACE ( 'NONE', #4578, 5.575000000000000178 ) ;
#9308=EDGE_CURVE ( 'NONE', #2369, #828, #16466, .T. ) ;
#9342=CYLINDRICAL_SURFACE ( 'NONE', #14748, 5.400000000000000355 ) ;
#9369=VECTOR ( 'NONE', #4035, 1000.000000000000000 ) ;
#9380=ADVANCED_FACE ( 'NONE', ( #4435, #2966 ), #8930, .T. ) ;
#9414=CIRCLE ( 'NONE', #14426, 5.400000000000000355 ) ;
#9425=AXIS2_PLACEMENT_3D ( 'NONE', #11437, #1252, #16159 ) ;
#9480=EDGE_CURVE ( 'NONE', #2843, #17538, #9551, .T. ) ;
#9502=CARTESIAN_POINT ( 'NONE',  ( -1.149999999999998135, 5.021051876504148371E-16, 4.100000000000000533 ) ) ;
#9503=CIRCLE ( 'NONE', #3572, 0.5999999999999998668 ) ;
#9517=FILL_AREA_STYLE_COLOUR ( '', #1231 ) ;
#9527=FACE_OUTER_BOUND ( 'NONE', #11652, .T. ) ;
#9541=FACE_OUTER_BOUND ( 'NONE', #14419, .T. ) ;
#9551=CIRCLE ( 'NONE', #12367, 5.899999999999999467 ) ;
#9561=ORIENTED_EDGE ( 'NONE', *, *, #9308, .F. ) ;
#9562=DIRECTION ( 'NONE',  ( 0.000000000000000000, 0.000000000000000000, 1.000000000000000000 ) ) ;
#9620=DIRECTION ( 'NONE',  ( 1.000000000000000000, 0.000000000000000000, 0.000000000000000000 ) ) ;
#9636=ORIENTED_EDGE ( 'NONE', *, *, #9762, .T. ) ;
#9645=VERTEX_POINT ( 'NONE', #10084 ) ;
#9661=DIRECTION ( 'NONE',  ( 0.000000000000000000, 1.000000000000000000, -1.224646799147353207E-16 ) ) ;
#9686=AXIS2_PLACEMENT_3D ( 'NONE', #17001, #15510, #2085 ) ;
#9692=AXIS2_PLACEMENT_3D ( 'NONE', #13856, #8066, #18593 ) ;
#9729=TOROIDAL_SURFACE ( 'NONE', #13187, 4.100000000000000533, 0.1000000000000001582 ) ;
#9762=EDGE_CURVE ( 'NONE', #2296, #828, #11762, .T. ) ;
#9772=ORIENTED_EDGE ( 'NONE', *, *, #4420, .F. ) ;
#9794=ADVANCED_FACE ( 'NONE', ( #14984 ), #9282, .F. ) ;
#9865=DIRECTION ( 'NONE',  ( 0.000000000000000000, 0.000000000000000000, -1.000000000000000000 ) ) ;
#9876=ORIENTED_EDGE ( 'NONE', *, *, #14553, .T. ) ;
#9901=ORIENTED_EDGE ( 'NONE', *, *, #9480, .T. ) ;
#9968=CARTESIAN_POINT ( 'NONE',  ( -0.4472135954999577612, 5.633375276077824112E-16, 4.599999999999999645 ) ) ;
#10008=AXIS2_PLACEMENT_3D ( 'NONE', #4909, #1883, #7850 ) ;
#10016=AXIS2_PLACEMENT_3D ( 'NONE', #14752, #1336, #7310 ) ;
#10034=EDGE_CURVE ( 'NONE', #18478, #18720, #818, .T. ) ;
#10045=DIRECTION ( 'NONE',  ( 0.000000000000000000, 0.000000000000000000, -1.000000000000000000 ) ) ;
#10065=ORIENTED_EDGE ( 'NONE', *, *, #6993, .F. ) ;
#10084=CARTESIAN_POINT ( 'NONE',  ( -1.250000000000001110, 6.827405905246494173E-16, 5.575000000000000178 ) ) ;
#10105=ORIENTED_EDGE ( 'NONE', *, *, #16414, .T. ) ;
#10140=AXIS2_PLACEMENT_3D ( 'NONE', #1310, #4241, #11586 ) ;
#10173=DIRECTION ( 'NONE',  ( 1.000000000000000000, 0.000000000000000000, 0.000000000000000000 ) ) ;
#10214=ORIENTED_EDGE ( 'NONE', *, *, #6869, .F. ) ;
#10239=FACE_OUTER_BOUND ( 'NONE', #13398, .T. ) ;
#10242=DIRECTION ( 'NONE',  ( -1.000000000000000000, -0.000000000000000000, -0.000000000000000000 ) ) ;
#10252=CARTESIAN_POINT ( 'NONE',  ( -1.250000000000001110, 0.000000000000000000, 0.000000000000000000 ) ) ;
#10314=CARTESIAN_POINT ( 'NONE',  ( -0.1713913650100259145, 0.000000000000000000, 0.000000000000000000 ) ) ;
#10316=CARTESIAN_POINT ( 'NONE',  ( 0.1713913650100259145, 6.016077400811372436E-16, -4.424999999999999822 ) ) ;
#10358=DIRECTION ( 'NONE',  ( 1.000000000000000000, 0.000000000000000000, 0.000000000000000000 ) ) ;
#10359=AXIS2_PLACEMENT_3D ( 'NONE', #2871, #8834, #16191 ) ;
#10368=CIRCLE ( 'NONE', #19167, 4.100000000000000533 ) ;
#10413=DIRECTION ( 'NONE',  ( 1.000000000000000000, 0.000000000000000000, 0.000000000000000000 ) ) ;
#10420=EDGE_LOOP ( 'NONE', ( #17696, #9772, #15926, #15665 ) ) ;
#10432=DIRECTION ( 'NONE',  ( 0.000000000000000000, 0.000000000000000000, -1.000000000000000000 ) ) ;
#10444=DIRECTION ( 'NONE',  ( 0.000000000000000000, 0.000000000000000000, 1.000000000000000000 ) ) ;
#10465=DIRECTION ( 'NONE',  ( 0.000000000000000000, 1.000000000000000000, -1.224646799147353207E-16 ) ) ;
#10589=CIRCLE ( 'NONE', #18756, 4.599999999999999645 ) ;
#10626=TOROIDAL_SURFACE ( 'NONE', #17539, 5.899999999999999467, 0.1000000000000010186 ) ;
#10634=DIRECTION ( 'NONE',  ( 1.000000000000000000, 0.000000000000000000, 0.000000000000000000 ) ) ;
#10638=EDGE_CURVE ( 'NONE', #16268, #15764, #19136, .T. ) ;
#10653=ORIENTED_EDGE ( 'NONE', *, *, #8244, .T. ) ;
#10674=DIRECTION ( 'NONE',  ( -1.000000000000000000, 0.000000000000000000, -0.000000000000000000 ) ) ;
#10685=DIRECTION ( 'NONE',  ( 0.000000000000000000, 0.000000000000000000, -1.000000000000000000 ) ) ;
#10708=EDGE_CURVE ( 'NONE', #228, #6680, #12234, .T. ) ;
#10719=DIRECTION ( 'NONE',  ( 0.000000000000000000, 0.000000000000000000, -1.000000000000000000 ) ) ;
#10769=CIRCLE ( 'NONE', #18001, 4.100000000000000533 ) ;
#10844=EDGE_LOOP ( 'NONE', ( #378, #8019, #8662, #14936 ) ) ;
#10859=FACE_OUTER_BOUND ( 'NONE', #9168, .T. ) ;
#10869=CIRCLE ( 'NONE', #5888, 4.100000000000000533 ) ;
#10894=DIRECTION ( 'NONE',  ( -1.000000000000000000, -0.000000000000000000, -0.000000000000000000 ) ) ;
#10896=CARTESIAN_POINT ( 'NONE',  ( -1.150000000000001688, 7.347880794884120722E-16, 6.000000000000001776 ) ) ;
#10901=DIRECTION ( 'NONE',  ( 1.000000000000000000, 0.000000000000000000, 0.000000000000000000 ) ) ;
#10963=CIRCLE ( 'NONE', #4403, 5.400000000000000355 ) ;
#10989=ADVANCED_FACE ( 'NONE', ( #333 ), #12538, .T. ) ;
#11023=ORIENTED_EDGE ( 'NONE', *, *, #17341, .T. ) ;
#11046=DIRECTION ( 'NONE',  ( 1.000000000000000000, 0.000000000000000000, 0.000000000000000000 ) ) ;
#11062=EDGE_CURVE ( 'NONE', #18720, #18478, #9414, .T. ) ;
#11083=AXIS2_PLACEMENT_3D ( 'NONE', #3932, #5291, #12939 ) ;
#11115=ORIENTED_EDGE ( 'NONE', *, *, #18657, .F. ) ;
#11134=ORIENTED_EDGE ( 'NONE', *, *, #4892, .T. ) ;
#11180=EDGE_CURVE ( 'NONE', #2296, #18086, #10368, .T. ) ;
#11198=ADVANCED_FACE ( 'NONE', ( #15862 ), #9729, .T. ) ;
#11236=DIRECTION ( 'NONE',  ( 0.000000000000000000, 0.000000000000000000, -1.000000000000000000 ) ) ;
#11239=ORIENTED_EDGE ( 'NONE', *, *, #11901, .F. ) ;
#11297=EDGE_CURVE ( 'NONE', #8220, #5480, #1059, .T. ) ;
#11303=EDGE_LOOP ( 'NONE', ( #4095, #13292, #11134, #5705 ) ) ;
#11304=EDGE_CURVE ( 'NONE', #2993, #12017, #6601, .T. ) ;
#11305=ORIENTED_EDGE ( 'NONE', *, *, #10638, .F. ) ;
#11309=EDGE_CURVE ( 'NONE', #3228, #9645, #989, .T. ) ;
#11328=CARTESIAN_POINT ( 'NONE',  ( -1.250000000000001110, 7.286648454926751965E-16, 5.899999999999999467 ) ) ;
#11349=EDGE_CURVE ( 'NONE', #15181, #18044, #12564, .T. ) ;
#11360=ADVANCED_FACE ( 'NONE', ( #6053 ), #17274, .T. ) ;
#11402=DIRECTION ( 'NONE',  ( 0.000000000000000000, 0.000000000000000000, -1.000000000000000000 ) ) ;
#11437=CARTESIAN_POINT ( 'NONE',  ( -1.149999999999998135, 0.000000000000000000, 0.000000000000000000 ) ) ;
#11525=ORIENTED_EDGE ( 'NONE', *, *, #5311, .F. ) ;
#11586=DIRECTION ( 'NONE',  ( 0.000000000000000000, 0.000000000000000000, -1.000000000000000000 ) ) ;
#11589=EDGE_CURVE ( 'NONE', #228, #7385, #665, .T. ) ;
#11612=DIRECTION ( 'NONE',  ( 0.000000000000000000, 0.000000000000000000, -1.000000000000000000 ) ) ;
#11646=DIRECTION ( 'NONE',  ( 0.000000000000000000, 0.000000000000000000, -1.000000000000000000 ) ) ;
#11650=AXIS2_PLACEMENT_3D ( 'NONE', #9240, #18099, #10719 ) ;
#11652=EDGE_LOOP ( 'NONE', ( #8570, #7651, #2733, #16689 ) ) ;
#11743=ORIENTED_EDGE ( 'NONE', *, *, #8244, .F. ) ;
#11755=LINE ( 'NONE', #7063, #9369 ) ;
#11762=CIRCLE ( 'NONE', #2387, 0.1000000000000002554 ) ;
#11889=CIRCLE ( 'NONE', #9692, 4.599999999999999645 ) ;
#11901=EDGE_CURVE ( 'NONE', #5480, #3706, #3354, .T. ) ;
#11917=DIRECTION ( 'NONE',  ( 1.000000000000000000, 0.000000000000000000, 0.000000000000000000 ) ) ;
#11971=DIRECTION ( 'NONE',  ( 1.000000000000000000, 0.000000000000000000, 0.000000000000000000 ) ) ;
#12013=PRODUCT_DEFINITION ( 'UNKNOWN', '', #13555, #13984 ) ;
#12014=DIRECTION ( 'NONE',  ( 0.000000000000000000, 0.000000000000000000, 1.000000000000000000 ) ) ;
#12017=VERTEX_POINT ( 'NONE', #7296 ) ;
#12031=ORIENTED_EDGE ( 'NONE', *, *, #12644, .F. ) ;
#12095=DIRECTION ( 'NONE',  ( 0.000000000000000000, 0.000000000000000000, -1.000000000000000000 ) ) ;
#12098=DIRECTION ( 'NONE',  ( 1.000000000000000000, 0.000000000000000000, 0.000000000000000000 ) ) ;
#12099=CARTESIAN_POINT ( 'NONE',  ( 1.149999999999998135, 0.000000000000000000, 0.000000000000000000 ) ) ;
#12135=DIRECTION ( 'NONE',  ( 1.000000000000000000, 0.000000000000000000, 0.000000000000000000 ) ) ;
#12213=AXIS2_PLACEMENT_3D ( 'NONE', #692, #18648, #2644 ) ;
#12234=CIRCLE ( 'NONE', #17261, 5.899999999999999467 ) ;
#12254=VERTEX_POINT ( 'NONE', #10896 ) ;
#12275=ADVANCED_FACE ( 'NONE', ( #17487 ), #19066, .F. ) ;
#12349=DIRECTION ( 'NONE',  ( -1.000000000000000000, 0.000000000000000000, -0.000000000000000000 ) ) ;
#12367=AXIS2_PLACEMENT_3D ( 'NONE', #3445, #16983, #12640 ) ;
#12430=DIRECTION ( 'NONE',  ( -0.000000000000000000, 0.000000000000000000, 1.000000000000000000 ) ) ;
#12449=CARTESIAN_POINT ( 'NONE',  ( -1.250000000000001110, 0.000000000000000000, -5.899999999999999467 ) ) ;
#12470=CIRCLE ( 'NONE', #8733, 0.5999999999999998668 ) ;
#12538=TOROIDAL_SURFACE ( 'NONE', #7853, 5.000000000000000000, 0.5999999999999999778 ) ;
#12548=ORIENTED_EDGE ( 'NONE', *, *, #7720, .T. ) ;
#12549=ADVANCED_FACE ( 'NONE', ( #17556 ), #18413, .T. ) ;
#12555=AXIS2_PLACEMENT_3D ( 'NONE', #7594, #12098, #13855 ) ;
#12564=CIRCLE ( 'NONE', #14111, 5.400000000000000355 ) ;
#12640=DIRECTION ( 'NONE',  ( 0.000000000000000000, 0.000000000000000000, -1.000000000000000000 ) ) ;
#12644=EDGE_CURVE ( 'NONE', #12254, #2647, #16794, .T. ) ;
#12674=AXIS2_PLACEMENT_3D ( 'NONE', #9502, #4730, #6467 ) ;
#12686=ORIENTED_EDGE ( 'NONE', *, *, #16414, .F. ) ;
#12713=EDGE_LOOP ( 'NONE', ( #8206, #14888 ) ) ;
#12734=ADVANCED_FACE ( 'NONE', ( #18571 ), #13741, .T. ) ;
#12781=EDGE_LOOP ( 'NONE', ( #12031, #14342, #5522, #14318 ) ) ;
#12783=ORIENTED_EDGE ( 'NONE', *, *, #18774, .F. ) ;
#12837=AXIS2_PLACEMENT_3D ( 'NONE', #12099, #6039, #18107 ) ;
#12878=AXIS2_PLACEMENT_3D ( 'NONE', #9075, #6140, #10444 ) ;
#12939=DIRECTION ( 'NONE',  ( 0.000000000000000000, 0.000000000000000000, -1.000000000000000000 ) ) ;
#13011=DIRECTION ( 'NONE',  ( 1.000000000000000000, 0.000000000000000000, 0.000000000000000000 ) ) ;
#13068=DIRECTION ( 'NONE',  ( 0.000000000000000000, 0.000000000000000000, -1.000000000000000000 ) ) ;
#13137=CYLINDRICAL_SURFACE ( 'NONE', #11083, 4.000000000000000000 ) ;
#13147=TOROIDAL_SURFACE ( 'NONE', #12837, 4.100000000000000533, 0.1000000000000001582 ) ;
#13187=AXIS2_PLACEMENT_3D ( 'NONE', #963, #3906, #6936 ) ;
#13192=DIRECTION ( 'NONE',  ( 1.000000000000000000, 0.000000000000000000, 0.000000000000000000 ) ) ;
#13207=FACE_OUTER_BOUND ( 'NONE', #14450, .T. ) ;
#13229=DIRECTION ( 'NONE',  ( 0.000000000000000000, 0.000000000000000000, -1.000000000000000000 ) ) ;
#13292=ORIENTED_EDGE ( 'NONE', *, *, #361, .T. ) ;
#13306=CIRCLE ( 'NONE', #12674, 0.1000000000000002554 ) ;
#13332=EDGE_CURVE ( 'NONE', #16243, #6353, #10589, .T. ) ;
#13345=LINE ( 'NONE', #6014, #6098 ) ;
#13368=EDGE_LOOP ( 'NONE', ( #16417, #17513, #3877, #11239 ) ) ;
#13398=EDGE_LOOP ( 'NONE', ( #18376, #19286, #3484, #12783 ) ) ;
#13412=APPLICATION_CONTEXT ( 'automotive_design' ) ;
#13418=EDGE_LOOP ( 'NONE', ( #1212, #17615, #9046, #13971 ) ) ;
#13472=CARTESIAN_POINT ( 'NONE',  ( 1.249999999999997558, 0.000000000000000000, 0.000000000000000000 ) ) ;
#13486=FACE_OUTER_BOUND ( 'NONE', #18304, .T. ) ;
#13530=DIRECTION ( 'NONE',  ( 1.000000000000000000, 0.000000000000000000, 0.000000000000000000 ) ) ;
#13543=ORIENTED_EDGE ( 'NONE', *, *, #8673, .F. ) ;
#13544=DIRECTION ( 'NONE',  ( 1.000000000000000000, 0.000000000000000000, 0.000000000000000000 ) ) ;
#13555=PRODUCT_DEFINITION_FORMATION_WITH_SPECIFIED_SOURCE ( 'ANY', '', #4453, .NOT_KNOWN. ) ;
#13611=ORIENTED_EDGE ( 'NONE', *, *, #17341, .F. ) ;
#13623=DIRECTION ( 'NONE',  ( 1.000000000000000000, 0.000000000000000000, 0.000000000000000000 ) ) ;
#13650=( NAMED_UNIT ( * ) SI_UNIT ( $, .STERADIAN. ) SOLID_ANGLE_UNIT ( ) );
#13666=CARTESIAN_POINT ( 'NONE',  ( 1.250000000000001110, 0.000000000000000000, 0.000000000000000000 ) ) ;
#13698=ADVANCED_FACE ( 'NONE', ( #4791 ), #17510, .T. ) ;
#13703=AXIS2_PLACEMENT_3D ( 'NONE', #4079, #5740, #10045 ) ;
#13741=CYLINDRICAL_SURFACE ( 'NONE', #17168, 4.599999999999999645 ) ;
#13762=DIRECTION ( 'NONE',  ( 0.000000000000000000, 0.000000000000000000, -1.000000000000000000 ) ) ;
#13792=DIRECTION ( 'NONE',  ( 0.000000000000000000, -1.224646799147353207E-16, 1.000000000000000000 ) ) ;
#13840=EDGE_CURVE ( 'NONE', #16268, #16243, #12470, .T. ) ;
#13855=DIRECTION ( 'NONE',  ( 0.000000000000000000, 0.000000000000000000, -1.000000000000000000 ) ) ;
#13856=CARTESIAN_POINT ( 'NONE',  ( -1.249999999999997558, 0.000000000000000000, 0.000000000000000000 ) ) ;
#13865=EDGE_CURVE ( 'NONE', #2993, #828, #951, .T. ) ;
#13886=CARTESIAN_POINT ( 'NONE',  ( 1.250000000000001110, 0.000000000000000000, 0.000000000000000000 ) ) ;
#13894=PLANE ( 'NONE',  #4847 ) ;
#13923=SURFACE_STYLE_FILL_AREA ( #16797 ) ;
#13930=EDGE_CURVE ( 'NONE', #2647, #2843, #19408, .T. ) ;
#13935=LINE ( 'NONE', #8054, #4831 ) ;
#13965=DIRECTION ( 'NONE',  ( 0.000000000000000000, 0.000000000000000000, -1.000000000000000000 ) ) ;
#13971=ORIENTED_EDGE ( 'NONE', *, *, #11349, .T. ) ;
#13980=DIRECTION ( 'NONE',  ( 0.000000000000000000, 0.000000000000000000, -1.000000000000000000 ) ) ;
#13984=PRODUCT_DEFINITION_CONTEXT ( 'detailed design', #13412, 'design' ) ;
#13988=EDGE_CURVE ( 'NONE', #6680, #12254, #9037, .T. ) ;
#14001=ORIENTED_EDGE ( 'NONE', *, *, #14553, .F. ) ;
#14002=DIRECTION ( 'NONE',  ( -0.000000000000000000, 0.000000000000000000, 1.000000000000000000 ) ) ;
#14029=DIRECTION ( 'NONE',  ( 1.000000000000000000, 0.000000000000000000, 0.000000000000000000 ) ) ;
#14047=AXIS2_PLACEMENT_3D ( 'NONE', #15239, #1820, #18399 ) ;
#14080=VECTOR ( 'NONE', #11971, 1000.000000000000000 ) ;
#14087=CIRCLE ( 'NONE', #5012, 0.1000000000000011297 ) ;
#14111=AXIS2_PLACEMENT_3D ( 'NONE', #17929, #1444, #14865 ) ;
#14118=CARTESIAN_POINT ( 'NONE',  ( -20.63749999999999574, 7.347880794884121708E-16, 6.000000000000001776 ) ) ;
#14132=DIRECTION ( 'NONE',  ( 0.000000000000000000, 0.000000000000000000, -1.000000000000000000 ) ) ;
#14139=DIRECTION ( 'NONE',  ( 1.000000000000000000, 0.000000000000000000, 0.000000000000000000 ) ) ;
#14146=ADVANCED_FACE ( 'NONE', ( #7506 ), #8095, .T. ) ;
#14224=DIRECTION ( 'NONE',  ( 1.000000000000000000, 0.000000000000000000, 0.000000000000000000 ) ) ;
#14266=CARTESIAN_POINT ( 'NONE',  ( 1.150000000000000577, 7.225416114969384193E-16, 5.899999999999999467 ) ) ;
#14309=ADVANCED_FACE ( 'NONE', ( #18212 ), #7888, .F. ) ;
#14318=ORIENTED_EDGE ( 'NONE', *, *, #15982, .F. ) ;
#14321=AXIS2_PLACEMENT_3D ( 'NONE', #6219, #15231, #12095 ) ;
#14333=MECHANICAL_DESIGN_GEOMETRIC_PRESENTATION_REPRESENTATION('',(#18133),#15918);
#14336=CARTESIAN_POINT ( 'NONE',  ( 1.149999999999998135, 0.000000000000000000, 0.000000000000000000 ) ) ;
#14342=ORIENTED_EDGE ( 'NONE', *, *, #2477, .T. ) ;
#14365=CIRCLE ( 'NONE', #1876, 5.575000000000000178 ) ;
#14373=ORIENTED_EDGE ( 'NONE', *, *, #13865, .T. ) ;
#14375=ORIENTED_EDGE ( 'NONE', *, *, #16204, .T. ) ;
#14388=ORIENTED_EDGE ( 'NONE', *, *, #8713, .T. ) ;
#14400=CARTESIAN_POINT ( 'NONE',  ( -20.63749999999999929, 0.000000000000000000, 0.000000000000000000 ) ) ;
#14419=EDGE_LOOP ( 'NONE', ( #6722, #6822, #43, #15476 ) ) ;
#14426=AXIS2_PLACEMENT_3D ( 'NONE', #15667, #11046, #13980 ) ;
#14450=EDGE_LOOP ( 'NONE', ( #7601, #3603, #16134, #18166 ) ) ;
#14473=ORIENTED_EDGE ( 'NONE', *, *, #11062, .T. ) ;
#14553=EDGE_CURVE ( 'NONE', #15764, #16268, #14365, .T. ) ;
#14605=CIRCLE ( 'NONE', #8659, 0.1000000000000002554 ) ;
#14674=CARTESIAN_POINT ( 'NONE',  ( -20.63749999999999929, 0.000000000000000000, -4.599999999999999645 ) ) ;
#14694=DIRECTION ( 'NONE',  ( 1.000000000000000000, 0.000000000000000000, 0.000000000000000000 ) ) ;
#14747=VECTOR ( 'NONE', #13011, 1000.000000000000000 ) ;
#14748=AXIS2_PLACEMENT_3D ( 'NONE', #3379, #3201, #13762 ) ;
#14752=CARTESIAN_POINT ( 'NONE',  ( 1.150000000000000577, 0.000000000000000000, 0.000000000000000000 ) ) ;
#14829=ORIENTED_EDGE ( 'NONE', *, *, #16944, .T. ) ;
#14861=CIRCLE ( 'NONE', #19291, 4.000000000000000000 ) ;
#14865=DIRECTION ( 'NONE',  ( 0.000000000000000000, 0.000000000000000000, 1.000000000000000000 ) ) ;
#14877=VECTOR ( 'NONE', #16554, 1000.000000000000000 ) ;
#14888=ORIENTED_EDGE ( 'NONE', *, *, #19157, .F. ) ;
#14912=CARTESIAN_POINT ( 'NONE',  ( -1.250000000000000666, 5.575000000000000178, 0.000000000000000000 ) ) ;
#14936=ORIENTED_EDGE ( 'NONE', *, *, #8789, .T. ) ;
#14973=ORIENTED_EDGE ( 'NONE', *, *, #10034, .F. ) ;
#14979=MANIFOLD_SOLID_BREP ( 'OuterRace', #524 ) ;
#14984=FACE_OUTER_BOUND ( 'NONE', #18431, .T. ) ;
#15005=TOROIDAL_SURFACE ( 'NONE', #18787, 5.899999999999999467, 0.1000000000000010186 ) ;
#15123=DIRECTION ( 'NONE',  ( 1.000000000000000000, 0.000000000000000000, 0.000000000000000000 ) ) ;
#15124=SHAPE_REPRESENTATION_RELATIONSHIP ( 'NONE' , 'NONE' ,  #18081, #8234 ) ;
#15181=VERTEX_POINT ( 'NONE', #4970 ) ;
#15183=UNCERTAINTY_MEASURE_WITH_UNIT (LENGTH_MEASURE( 1.000000000000000082E-05 ), #17088, 'distance_accuracy_value', 'NONE');
#15201=CARTESIAN_POINT ( 'NONE',  ( 1.149999999999998135, 0.000000000000000000, 0.000000000000000000 ) ) ;
#15231=DIRECTION ( 'NONE',  ( 1.000000000000000000, 0.000000000000000000, 0.000000000000000000 ) ) ;
#15239=CARTESIAN_POINT ( 'NONE',  ( -20.63749999999999574, 0.000000000000000000, 0.000000000000000000 ) ) ;
#15273=CIRCLE ( 'NONE', #14321, 4.599999999999999645 ) ;
#15318=STYLED_ITEM ( 'NONE', ( #1701 ), #8234 ) ;
#15322=CIRCLE ( 'NONE', #17213, 6.000000000000000888 ) ;
#15349=EDGE_LOOP ( 'NONE', ( #16058, #18422, #6211, #3191 ) ) ;
#15443=CARTESIAN_POINT ( 'NONE',  ( -1.150000000000000577, 0.000000000000000000, -5.899999999999999467 ) ) ;
#15476=ORIENTED_EDGE ( 'NONE', *, *, #2477, .F. ) ;
#15502=CARTESIAN_POINT ( 'NONE',  ( -20.63749999999999929, 0.000000000000000000, 0.000000000000000000 ) ) ;
#15504=( NAMED_UNIT ( * ) SI_UNIT ( $, .STERADIAN. ) SOLID_ANGLE_UNIT ( ) );
#15510=DIRECTION ( 'NONE',  ( 1.000000000000000000, 0.000000000000000000, 0.000000000000000000 ) ) ;
#15557=TOROIDAL_SURFACE ( 'NONE', #19027, 4.100000000000000533, 0.1000000000000001582 ) ;
#15615=DIRECTION ( 'NONE',  ( 0.000000000000000000, 0.000000000000000000, -1.000000000000000000 ) ) ;
#15649=ADVANCED_FACE ( 'NONE', ( #9541 ), #15005, .T. ) ;
#15665=ORIENTED_EDGE ( 'NONE', *, *, #9308, .T. ) ;
#15667=CARTESIAN_POINT ( 'NONE',  ( 1.250000000000001110, 0.000000000000000000, 0.000000000000000000 ) ) ;
#15739=DIRECTION ( 'NONE',  ( 0.000000000000000000, 0.000000000000000000, -1.000000000000000000 ) ) ;
#15764=VERTEX_POINT ( 'NONE', #6134 ) ;
#15811=DIRECTION ( 'NONE',  ( 0.000000000000000000, 0.000000000000000000, -1.000000000000000000 ) ) ;
#15818=DIRECTION ( 'NONE',  ( 0.000000000000000000, -1.000000000000000000, 0.000000000000000000 ) ) ;
#15862=FACE_OUTER_BOUND ( 'NONE', #17381, .T. ) ;
#15918=( GEOMETRIC_REPRESENTATION_CONTEXT ( 3 ) GLOBAL_UNCERTAINTY_ASSIGNED_CONTEXT ( ( #17753 ) ) GLOBAL_UNIT_ASSIGNED_CONTEXT ( ( #3035, #1459, #16468 ) ) REPRESENTATION_CONTEXT ( 'NONE', 'WORKASPACE' ) );
#15926=ORIENTED_EDGE ( 'NONE', *, *, #3886, .T. ) ;
#15933=AXIS2_PLACEMENT_3D ( 'NONE', #1947, #6530, #9562 ) ;
#15950=CARTESIAN_POINT ( 'NONE',  ( -1.150000000000000577, 7.225416114969384193E-16, 5.899999999999999467 ) ) ;
#15963=CIRCLE ( 'NONE', #4064, 0.1000000000000002554 ) ;
#15982=EDGE_CURVE ( 'NONE', #2647, #8711, #15322, .T. ) ;
#15987=FACE_OUTER_BOUND ( 'NONE', #10420, .T. ) ;
#16030=VERTEX_POINT ( 'NONE', #10316 ) ;
#16058=ORIENTED_EDGE ( 'NONE', *, *, #4420, .T. ) ;
#16134=ORIENTED_EDGE ( 'NONE', *, *, #18774, .T. ) ;
#16145=DIRECTION ( 'NONE',  ( 1.000000000000000000, 0.000000000000000000, 0.000000000000000000 ) ) ;
#16159=DIRECTION ( 'NONE',  ( 0.000000000000000000, 0.000000000000000000, -1.000000000000000000 ) ) ;
#16168=AXIS2_PLACEMENT_3D ( 'NONE', #13886, #5265, #11236 ) ;
#16191=DIRECTION ( 'NONE',  ( 1.000000000000000000, 0.000000000000000000, 0.000000000000000000 ) ) ;
#16197=AXIS2_PLACEMENT_3D ( 'NONE', #17388, #14224, #15811 ) ;
#16204=EDGE_CURVE ( 'NONE', #9645, #3228, #7819, .T. ) ;
#16243=VERTEX_POINT ( 'NONE', #17187 ) ;
#16268=VERTEX_POINT ( 'NONE', #8149 ) ;
#16277=AXIS2_PLACEMENT_3D ( 'NONE', #2915, #10242, #5747 ) ;
#16284=ADVANCED_FACE ( 'NONE', ( #3848 ), #10626, .T. ) ;
#16307=DIRECTION ( 'NONE',  ( 0.000000000000000000, 0.000000000000000000, -1.000000000000000000 ) ) ;
#16332=FACE_BOUND ( 'NONE', #6842, .T. ) ;
#16335=CIRCLE ( 'NONE', #6914, 5.899999999999999467 ) ;
#16358=ADVANCED_FACE ( 'NONE', ( #17092 ), #6973, .T. ) ;
#16414=EDGE_CURVE ( 'NONE', #18086, #2369, #15963, .T. ) ;
#16417=ORIENTED_EDGE ( 'NONE', *, *, #11297, .F. ) ;
#16436=PLANE ( 'NONE',  #7196 ) ;
#16464=ORIENTED_EDGE ( 'NONE', *, *, #13988, .T. ) ;
#16466=CIRCLE ( 'NONE', #5175, 4.000000000000000000 ) ;
#16468=( NAMED_UNIT ( * ) SI_UNIT ( $, .STERADIAN. ) SOLID_ANGLE_UNIT ( ) );
#16534=ORIENTED_EDGE ( 'NONE', *, *, #6869, .T. ) ;
#16554=DIRECTION ( 'NONE',  ( 1.000000000000000000, 0.000000000000000000, 0.000000000000000000 ) ) ;
#16616=AXIS2_PLACEMENT_3D ( 'NONE', #17026, #5139, #17316 ) ;
#16645=CARTESIAN_POINT ( 'NONE',  ( 0.4472135954999577612, 0.000000000000000000, 0.000000000000000000 ) ) ;
#16689=ORIENTED_EDGE ( 'NONE', *, *, #4892, .F. ) ;
#16710=EDGE_CURVE ( 'NONE', #6066, #6353, #6370, .T. ) ;
#16752=DIRECTION ( 'NONE',  ( -0.000000000000000000, 1.000000000000000000, 1.224646799147353207E-16 ) ) ;
#16760=EDGE_LOOP ( 'NONE', ( #19303, #384 ) ) ;
#16769=EDGE_CURVE ( 'NONE', #16030, #18044, #6892, .T. ) ;
#16794=LINE ( 'NONE', #14118, #6191 ) ;
#16797=FILL_AREA_STYLE ('',( #9517 ) ) ;
#16816=CARTESIAN_POINT ( 'NONE',  ( 1.150000000000001688, 0.000000000000000000, 0.000000000000000000 ) ) ;
#16832=DIRECTION ( 'NONE',  ( 0.000000000000000000, -1.000000000000000000, 0.000000000000000000 ) ) ;
#16897=CARTESIAN_POINT ( 'NONE',  ( -1.250000000000001110, 0.000000000000000000, 0.000000000000000000 ) ) ;
#16917=DIRECTION ( 'NONE',  ( 1.000000000000000000, 0.000000000000000000, 0.000000000000000000 ) ) ;
#16944=EDGE_CURVE ( 'NONE', #18044, #15181, #10963, .T. ) ;
#16983=DIRECTION ( 'NONE',  ( 1.000000000000000000, 0.000000000000000000, 0.000000000000000000 ) ) ;
#16998=SURFACE_SIDE_STYLE ('',( #13923 ) ) ;
#17001=CARTESIAN_POINT ( 'NONE',  ( -20.63749999999999574, 0.000000000000000000, 0.000000000000000000 ) ) ;
#17002=DIRECTION ( 'NONE',  ( 0.000000000000000000, 0.000000000000000000, 1.000000000000000000 ) ) ;
#17026=CARTESIAN_POINT ( 'NONE',  ( -0.1713913650100259145, 0.000000000000000000, 0.000000000000000000 ) ) ;
#17075=EDGE_CURVE ( 'NONE', #8220, #16030, #8771, .T. ) ;
#17088=( LENGTH_UNIT ( ) NAMED_UNIT ( * ) SI_UNIT ( .MILLI., .METRE. ) );
#17092=FACE_OUTER_BOUND ( 'NONE', #12781, .T. ) ;
#17136=DIRECTION ( 'NONE',  ( 0.000000000000000000, 1.224646799147351975E-16, 1.000000000000000000 ) ) ;
#17168=AXIS2_PLACEMENT_3D ( 'NONE', #15502, #1795, #705 ) ;
#17187=CARTESIAN_POINT ( 'NONE',  ( -0.4472135954999577612, 0.000000000000000000, -4.599999999999999645 ) ) ;
#17213=AXIS2_PLACEMENT_3D ( 'NONE', #4253, #1322, #8657 ) ;
#17233=TOROIDAL_SURFACE ( 'NONE', #10016, 5.899999999999999467, 0.1000000000000010186 ) ;
#17261=AXIS2_PLACEMENT_3D ( 'NONE', #831, #8473, #11402 ) ;
#17274=TOROIDAL_SURFACE ( 'NONE', #12878, 5.000000000000000000, 0.5999999999999999778 ) ;
#17316=DIRECTION ( 'NONE',  ( 0.000000000000000000, 0.000000000000000000, -1.000000000000000000 ) ) ;
#17338=DIRECTION ( 'NONE',  ( 1.000000000000000000, 0.000000000000000000, 0.000000000000000000 ) ) ;
#17341=EDGE_CURVE ( 'NONE', #7385, #12254, #7532, .T. ) ;
#17381=EDGE_LOOP ( 'NONE', ( #8212, #18083, #12548, #1872 ) ) ;
#17388=CARTESIAN_POINT ( 'NONE',  ( -20.63749999999999574, 0.000000000000000000, 0.000000000000000000 ) ) ;
#17390=EDGE_LOOP ( 'NONE', ( #6078, #8205, #10653, #1927 ) ) ;
#17419=CARTESIAN_POINT ( 'NONE',  ( 1.150000000000001688, 0.000000000000000000, -6.000000000000000888 ) ) ;
#17438=ORIENTED_EDGE ( 'NONE', *, *, #11309, .T. ) ;
#17439=DIRECTION ( 'NONE',  ( 0.000000000000000000, 0.000000000000000000, -1.000000000000000000 ) ) ;
#17442=ADVANCED_FACE ( 'NONE', ( #17752 ), #8718, .T. ) ;
#17487=FACE_OUTER_BOUND ( 'NONE', #8859, .T. ) ;
#17502=ORIENTED_EDGE ( 'NONE', *, *, #17075, .F. ) ;
#17510=TOROIDAL_SURFACE ( 'NONE', #15933, 5.000000000000000000, 0.5999999999999999778 ) ;
#17513=ORIENTED_EDGE ( 'NONE', *, *, #19377, .F. ) ;
#17538=VERTEX_POINT ( 'NONE', #4707 ) ;
#17539=AXIS2_PLACEMENT_3D ( 'NONE', #901, #18667, #8245 ) ;
#17556=FACE_OUTER_BOUND ( 'NONE', #4967, .T. ) ;
#17567=DIRECTION ( 'NONE',  ( 0.000000000000000000, 0.000000000000000000, -1.000000000000000000 ) ) ;
#17581=AXIS2_PLACEMENT_3D ( 'NONE', #2286, #3940, #8239 ) ;
#17594=EDGE_LOOP ( 'NONE', ( #9210, #14373, #1079, #8210 ) ) ;
#17615=ORIENTED_EDGE ( 'NONE', *, *, #19377, .T. ) ;
#17641=CARTESIAN_POINT ( 'NONE',  ( 1.249999999999997558, 0.000000000000000000, 0.000000000000000000 ) ) ;
#17692=DIRECTION ( 'NONE',  ( 0.000000000000000000, 0.000000000000000000, -1.000000000000000000 ) ) ;
#17696=ORIENTED_EDGE ( 'NONE', *, *, #13865, .F. ) ;
#17719=EDGE_LOOP ( 'NONE', ( #17502, #3899, #10065, #4348 ) ) ;
#17730=DIRECTION ( 'NONE',  ( 1.000000000000000000, 0.000000000000000000, 0.000000000000000000 ) ) ;
#17752=FACE_OUTER_BOUND ( 'NONE', #13368, .T. ) ;
#17753=UNCERTAINTY_MEASURE_WITH_UNIT (LENGTH_MEASURE( 1.000000000000000082E-05 ), #3035, 'distance_accuracy_value', 'NONE');
#17756=CARTESIAN_POINT ( 'NONE',  ( -1.149999999999998135, 0.000000000000000000, 0.000000000000000000 ) ) ;
#17775=CIRCLE ( 'NONE', #13703, 0.5999999999999998668 ) ;
#17810=EDGE_CURVE ( 'NONE', #3228, #16268, #2190, .T. ) ;
#17829=DIRECTION ( 'NONE',  ( 0.000000000000000000, 0.000000000000000000, -1.000000000000000000 ) ) ;
#17836=CARTESIAN_POINT ( 'NONE',  ( 1.249999999999997780, 5.021051876504148371E-16, 4.100000000000000533 ) ) ;
#17888=AXIS2_PLACEMENT_3D ( 'NONE', #5781, #2667, #8620 ) ;
#17929=CARTESIAN_POINT ( 'NONE',  ( 0.4472135954999577612, 0.000000000000000000, 0.000000000000000000 ) ) ;
#17950=CARTESIAN_POINT ( 'NONE',  ( 1.149999999999998135, 5.021051876504148371E-16, 4.100000000000000533 ) ) ;
#18001=AXIS2_PLACEMENT_3D ( 'NONE', #8158, #10901, #14132 ) ;
#18044=VERTEX_POINT ( 'NONE', #4145 ) ;
#18071=DIRECTION ( 'NONE',  ( 1.000000000000000000, 0.000000000000000000, 0.000000000000000000 ) ) ;
#18081=SHAPE_REPRESENTATION ( 'angular contact ball bearing_68_iso_ISO 15 ABB - 178 - 20,SI,NC,20_68', ( #10359 ), #1557 ) ;
#18083=ORIENTED_EDGE ( 'NONE', *, *, #11304, .T. ) ;
#18085=EDGE_CURVE ( 'NONE', #15181, #18720, #11755, .T. ) ;
#18086=VERTEX_POINT ( 'NONE', #1293 ) ;
#18099=DIRECTION ( 'NONE',  ( 1.000000000000000000, 0.000000000000000000, 0.000000000000000000 ) ) ;
#18107=DIRECTION ( 'NONE',  ( 0.000000000000000000, 0.000000000000000000, -1.000000000000000000 ) ) ;
#18123=DIRECTION ( 'NONE',  ( 1.000000000000000000, 0.000000000000000000, 0.000000000000000000 ) ) ;
#18133=STYLED_ITEM('',(#19468),#14979);
#18148=UNCERTAINTY_MEASURE_WITH_UNIT (LENGTH_MEASURE( 1.000000000000000082E-05 ), #18375, 'distance_accuracy_value', 'NONE');
#18155=CARTESIAN_POINT ( 'NONE',  ( -20.63749999999999574, 0.000000000000000000, -6.000000000000001776 ) ) ;
#18166=ORIENTED_EDGE ( 'NONE', *, *, #9480, .F. ) ;
#18206=DIRECTION ( 'NONE',  ( 0.000000000000000000, 0.000000000000000000, -1.000000000000000000 ) ) ;
#18212=FACE_OUTER_BOUND ( 'NONE', #4067, .T. ) ;
#18304=EDGE_LOOP ( 'NONE', ( #6655, #2252 ) ) ;
#18375=( LENGTH_UNIT ( ) NAMED_UNIT ( * ) SI_UNIT ( .MILLI., .METRE. ) );
#18376=ORIENTED_EDGE ( 'NONE', *, *, #18657, .T. ) ;
#18399=DIRECTION ( 'NONE',  ( 0.000000000000000000, 0.000000000000000000, -1.000000000000000000 ) ) ;
#18413=TOROIDAL_SURFACE ( 'NONE', #1489, 4.100000000000000533, 0.1000000000000001582 ) ;
#18419=CARTESIAN_POINT ( 'NONE',  ( 1.149999999999998135, 0.000000000000000000, -4.000000000000000000 ) ) ;
#18422=ORIENTED_EDGE ( 'NONE', *, *, #222, .T. ) ;
#18431=EDGE_LOOP ( 'NONE', ( #10214, #5758, #4117, #14001 ) ) ;
#18478=VERTEX_POINT ( 'NONE', #947 ) ;
#18490=CARTESIAN_POINT ( 'NONE',  ( 1.250000000000001110, 6.613092715395707467E-16, 5.400000000000000355 ) ) ;
#18492=ORIENTED_EDGE ( 'NONE', *, *, #16204, .F. ) ;
#18525=ADVANCED_FACE ( 'NONE', ( #13486, #1235 ), #16436, .T. ) ;
#18531=AXIS2_PLACEMENT_3D ( 'NONE', #14336, #14139, #8461 ) ;
#18554=ADVANCED_FACE ( 'NONE', ( #19205 ), #13147, .T. ) ;
#18571=FACE_OUTER_BOUND ( 'NONE', #11303, .T. ) ;
#18593=DIRECTION ( 'NONE',  ( 0.000000000000000000, 0.000000000000000000, -1.000000000000000000 ) ) ;
#18597=ORIENTED_EDGE ( 'NONE', *, *, #361, .F. ) ;
#18617=ORIENTED_EDGE ( 'NONE', *, *, #19024, .T. ) ;
#18637=ADVANCED_FACE ( 'NONE', ( #10239 ), #17233, .T. ) ;
#18647=EDGE_CURVE ( 'NONE', #19035, #6066, #11889, .T. ) ;
#18648=DIRECTION ( 'NONE',  ( -0.000000000000000000, 1.000000000000000000, 1.224646799147353207E-16 ) ) ;
#18653=CARTESIAN_POINT ( 'NONE',  ( 1.250000000000001110, 7.286648454926751965E-16, 5.899999999999999467 ) ) ;
#18657=EDGE_CURVE ( 'NONE', #8711, #2647, #3458, .T. ) ;
#18667=DIRECTION ( 'NONE',  ( 1.000000000000000000, 0.000000000000000000, 0.000000000000000000 ) ) ;
#18720=VERTEX_POINT ( 'NONE', #18490 ) ;
#18756=AXIS2_PLACEMENT_3D ( 'NONE', #4719, #582, #4902 ) ;
#18774=EDGE_CURVE ( 'NONE', #8711, #17538, #14087, .T. ) ;
#18787=AXIS2_PLACEMENT_3D ( 'NONE', #3210, #10634, #357 ) ;
#18794=VECTOR ( 'NONE', #2089, 1000.000000000000000 ) ;
#18862=ORIENTED_EDGE ( 'NONE', *, *, #5927, .F. ) ;
#19024=EDGE_CURVE ( 'NONE', #444, #6110, #30, .T. ) ;
#19027=AXIS2_PLACEMENT_3D ( 'NONE', #7565, #18071, #16307 ) ;
#19035=VERTEX_POINT ( 'NONE', #1211 ) ;
#19066=CYLINDRICAL_SURFACE ( 'NONE', #16197, 5.575000000000000178 ) ;
#19071=CARTESIAN_POINT ( 'NONE',  ( 0.000000000000000000, 0.000000000000000000, 5.000000000000000000 ) ) ;
#19136=CIRCLE ( 'NONE', #16616, 5.575000000000000178 ) ;
#19157=EDGE_CURVE ( 'NONE', #6680, #228, #2852, .T. ) ;
#19167=AXIS2_PLACEMENT_3D ( 'NONE', #17641, #17730, #17439 ) ;
#19168=CIRCLE ( 'NONE', #18531, 4.000000000000000000 ) ;
#19194=ORIENTED_EDGE ( 'NONE', *, *, #7051, .T. ) ;
#19205=FACE_OUTER_BOUND ( 'NONE', #8361, .T. ) ;
#19286=ORIENTED_EDGE ( 'NONE', *, *, #13930, .T. ) ;
#19291=AXIS2_PLACEMENT_3D ( 'NONE', #17756, #13530, #1676 ) ;
#19294=CARTESIAN_POINT ( 'NONE',  ( 1.149999999999998135, 4.959819536546779614E-16, 4.000000000000000000 ) ) ;
#19303=ORIENTED_EDGE ( 'NONE', *, *, #8713, .F. ) ;
#19377=EDGE_CURVE ( 'NONE', #16030, #8220, #6588, .T. ) ;
#19389=DIRECTION ( 'NONE',  ( 0.000000000000000000, 0.000000000000000000, -1.000000000000000000 ) ) ;
#19408=CIRCLE ( 'NONE', #7476, 0.1000000000000011297 ) ;
#19462=COLOUR_RGB('Grey',0.48,0.52,0.57);
#19463=FILL_AREA_STYLE_COLOUR('',#19462);
#19464=FILL_AREA_STYLE('',(#19463));
#19465=SURFACE_STYLE_FILL_AREA(#19464);
#19466=SURFACE_SIDE_STYLE('',(#19465));
#19467=SURFACE_STYLE_USAGE(.BOTH.,#19466);
#19468=PRESENTATION_STYLE_ASSIGNMENT((#19467));
ENDSEC;
END-ISO-10303-21;
